ISO-10303-21;
HEADER;
FILE_DESCRIPTION (('STEP AP214'),
    '1' );
FILE_NAME ('socket head cap screw_iso_ISO 4762 M5 x 16 - 16N.step',
    '2026-10-24T13:33:06',
    ( '' ),
    ( '' ),
    'SwSTEP 2.0',
    'SolidWorks 2026',
    '' );
FILE_SCHEMA (( 'AUTOMOTIVE_DESIGN' ));
ENDSEC;

DATA;
#11=EDGE_CURVE ( 'NONE', #2602, #678, #10776, .T. ) ;
#14=AXIS2_PLACEMENT_3D ( 'NONE', #7611, #4365, #10700 ) ;
#17=ORIENTED_EDGE ( 'NONE', *, *, #13765, .F. ) ;
#28=VECTOR ( 'NONE', #11250, 999.9999999999997726 ) ;
#43=CIRCLE ( 'NONE', #4245, 0.2000000000000000944 ) ;
#66=ORIENTED_EDGE ( 'NONE', *, *, #8156, .T. ) ;
#67=VERTEX_POINT ( 'NONE', #13720 ) ;
#71=CYLINDRICAL_SURFACE ( 'NONE', #9896, 2.500000000000000444 ) ;
#99=CARTESIAN_POINT ( 'NONE',  ( 4.999999999999997335, 0.000000000000000000, 4.250000000000000000 ) ) ;
#104=DIRECTION ( 'NONE',  ( 0.000000000000000000, 0.000000000000000000, 1.000000000000000000 ) ) ;
#118=ORIENTED_EDGE ( 'NONE', *, *, #14031, .F. ) ;
#123=ORIENTED_EDGE ( 'NONE', *, *, #13765, .T. ) ;
#147=DIRECTION ( 'NONE',  ( 0.000000000000000000, 0.000000000000000000, 1.000000000000000000 ) ) ;
#151=FACE_OUTER_BOUND ( 'NONE', #9117, .T. ) ;
#152=AXIS2_PLACEMENT_3D ( 'NONE', #10051, #218, #9907 ) ;
#170=ORIENTED_EDGE ( 'NONE', *, *, #8134, .F. ) ;
#172=CARTESIAN_POINT ( 'NONE',  ( 21.00000000000000355, 0.000000000000000000, 0.000000000000000000 ) ) ;
#198=ORIENTED_EDGE ( 'NONE', *, *, #12237, .T. ) ;
#199=AXIS2_PLACEMENT_3D ( 'NONE', #13030, #8676, #7512 ) ;
#215=ORIENTED_EDGE ( 'NONE', *, *, #12757, .F. ) ;
#218=DIRECTION ( 'NONE',  ( -1.000000000000000000, -0.000000000000000000, -0.000000000000000000 ) ) ;
#283=CARTESIAN_POINT ( 'NONE',  ( 2.500000000000000000, -1.178949249685214307, 2.042000000000001592 ) ) ;
#304=ORIENTED_EDGE ( 'NONE', *, *, #14182, .F. ) ;
#305=DIRECTION ( 'NONE',  ( -1.000000000000000000, -0.000000000000000000, -0.000000000000000000 ) ) ;
#309=ORIENTED_EDGE ( 'NONE', *, *, #12893, .T. ) ;
#317=DIRECTION ( 'NONE',  ( 0.000000000000000000, 0.000000000000000000, 1.000000000000000000 ) ) ;
#349=AXIS2_PLACEMENT_3D ( 'NONE', #5295, #9713, #11738 ) ;
#356=AXIS2_PLACEMENT_3D ( 'NONE', #11452, #7091, #11525 ) ;
#402=DIRECTION ( 'NONE',  ( -0.5000000000000051070, 1.060575238724903217E-16, -0.8660254037844355990 ) ) ;
#435=DIRECTION ( 'NONE',  ( 0.000000000000000000, 0.000000000000000000, 1.000000000000000000 ) ) ;
#476=COLOUR_RGB ( '',1.000000000000000000, 0.9490196078431372140, 0.9098039215686274384 ) ;
#588=CARTESIAN_POINT ( 'NONE',  ( 0.000000000000000000, -2.357898499370432166, 3.035766082959412415E-15 ) ) ;
#623=FILL_AREA_STYLE_COLOUR ( '', #476 ) ;
#635=LINE ( 'NONE', #10377, #5692 ) ;
#659=( LENGTH_UNIT ( ) NAMED_UNIT ( * ) SI_UNIT ( .MILLI., .METRE. ) );
#666=DIRECTION ( 'NONE',  ( -1.000000000000000000, -0.000000000000000000, -0.000000000000000000 ) ) ;
#667=ORIENTED_EDGE ( 'NONE', *, *, #11104, .F. ) ;
#678=VERTEX_POINT ( 'NONE', #7669 ) ;
#686=CIRCLE ( 'NONE', #9763, 2.500000000000000444 ) ;
#689=LINE ( 'NONE', #14053, #13631 ) ;
#711=ADVANCED_FACE ( 'NONE', ( #4494 ), #2218, .T. ) ;
#719=ORIENTED_EDGE ( 'NONE', *, *, #8532, .T. ) ;
#733=DIRECTION ( 'NONE',  ( 0.000000000000000000, 1.000000000000000000, -1.287488025362403787E-15 ) ) ;
#734=CARTESIAN_POINT ( 'NONE',  ( 0.2500000000000002220, 5.204748896376250699E-16, -4.250000000000000000 ) ) ;
#747=EDGE_CURVE ( 'NONE', #11219, #4789, #11024, .T. ) ;
#748=DIRECTION ( 'NONE',  ( 0.000000000000000000, 0.000000000000000000, 1.000000000000000000 ) ) ;
#757=UNCERTAINTY_MEASURE_WITH_UNIT (LENGTH_MEASURE( 1.000000000000000082E-05 ), #6447, 'distance_accuracy_value', 'NONE');
#762=( NAMED_UNIT ( * ) SI_UNIT ( $, .STERADIAN. ) SOLID_ANGLE_UNIT ( ) );
#795=LINE ( 'NONE', #13010, #2439 ) ;
#813=EDGE_LOOP ( 'NONE', ( #884, #4496, #11074, #5018, #198 ) ) ;
#848=CARTESIAN_POINT ( 'NONE',  ( 5.000000000000000888, 4.250000000000000000, 0.000000000000000000 ) ) ;
#849=VECTOR ( 'NONE', #2245, 1000.000000000000000 ) ;
#860=ORIENTED_EDGE ( 'NONE', *, *, #6657, .T. ) ;
#884=ORIENTED_EDGE ( 'NONE', *, *, #7027, .T. ) ;
#892=ORIENTED_EDGE ( 'NONE', *, *, #10216, .F. ) ;
#938=CARTESIAN_POINT ( 'NONE',  ( 0.000000000000000000, -1.178949249685214307, 2.042000000000001592 ) ) ;
#965=ORIENTED_EDGE ( 'NONE', *, *, #7027, .F. ) ;
#977=EDGE_CURVE ( 'NONE', #8679, #1004, #9030, .T. ) ;
#1002=EDGE_LOOP ( 'NONE', ( #13804, #4995 ) ) ;
#1004=VERTEX_POINT ( 'NONE', #11805 ) ;
#1019=AXIS2_PLACEMENT_3D ( 'NONE', #11624, #9453, #1674 ) ;
#1073=EDGE_LOOP ( 'NONE', ( #667, #1257, #1363 ) ) ;
#1083=ORIENTED_EDGE ( 'NONE', *, *, #13637, .F. ) ;
#1104=DIRECTION ( 'NONE',  ( -1.000000000000000000, -0.000000000000000000, -0.000000000000000000 ) ) ;
#1144=CARTESIAN_POINT ( 'NONE',  ( 2.500000000000000000, -2.629050547790028551E-15, -2.041999999999999815 ) ) ;
#1175=VECTOR ( 'NONE', #5759, 1000.000000000000000 ) ;
#1178=DIRECTION ( 'NONE',  ( 1.000000000000000000, 0.000000000000000000, 0.000000000000000000 ) ) ;
#1211=LINE ( 'NONE', #7951, #14259 ) ;
#1248=ADVANCED_BREP_SHAPE_REPRESENTATION ( '', ( #3687, #14039 ), #1895 ) ;
#1249=CARTESIAN_POINT ( 'NONE',  ( -31.74999999999995737, 0.000000000000000000, 0.000000000000000000 ) ) ;
#1257=ORIENTED_EDGE ( 'NONE', *, *, #1636, .T. ) ;
#1262=EDGE_CURVE ( 'NONE', #12287, #4042, #3951, .T. ) ;
#1311=AXIS2_PLACEMENT_3D ( 'NONE', #10625, #8428, #6047 ) ;
#1322=FACE_OUTER_BOUND ( 'NONE', #10618, .T. ) ;
#1339=DIRECTION ( 'NONE',  ( -1.000000000000000000, -0.000000000000000000, -0.000000000000000000 ) ) ;
#1359=LINE ( 'NONE', #2456, #10238 ) ;
#1363=ORIENTED_EDGE ( 'NONE', *, *, #4120, .F. ) ;
#1367=CIRCLE ( 'NONE', #11787, 2.700000000000000622 ) ;
#1384=CONICAL_SURFACE ( 'NONE', #6268, 2.055000000000000160, 0.7853981633974639331 ) ;
#1395=MECHANICAL_DESIGN_GEOMETRIC_PRESENTATION_REPRESENTATION('',(#10207),#1885);
#1401=ADVANCED_FACE ( 'NONE', ( #6687, #8934 ), #11047, .T. ) ;
#1434=FACE_OUTER_BOUND ( 'NONE', #10121, .T. ) ;
#1440=VECTOR ( 'NONE', #9291, 1000.000000000000114 ) ;
#1546=CARTESIAN_POINT ( 'NONE',  ( 21.00000000000000355, 0.000000000000000000, 0.000000000000000000 ) ) ;
#1549=DIRECTION ( 'NONE',  ( 1.000000000000000000, 0.000000000000000000, 0.000000000000000000 ) ) ;
#1577=ORIENTED_EDGE ( 'NONE', *, *, #11810, .T. ) ;
#1632=APPLICATION_CONTEXT ( 'automotive_design' ) ;
#1636=EDGE_CURVE ( 'NONE', #3478, #12287, #8116, .T. ) ;
#1644=PLANE ( 'NONE',  #356 ) ;
#1660=FACE_OUTER_BOUND ( 'NONE', #13209, .T. ) ;
#1674=DIRECTION ( 'NONE',  ( 0.000000000000000000, 0.000000000000000000, 1.000000000000000000 ) ) ;
#1701=FACE_OUTER_BOUND ( 'NONE', #8205, .T. ) ;
#1704=FACE_OUTER_BOUND ( 'NONE', #9597, .T. ) ;
#1730=CARTESIAN_POINT ( 'NONE',  ( 2.500000000000000000, 0.000000000000000000, 0.000000000000000000 ) ) ;
#1736=FACE_OUTER_BOUND ( 'NONE', #10449, .T. ) ;
#1744=ORIENTED_EDGE ( 'NONE', *, *, #2581, .T. ) ;
#1761=EDGE_CURVE ( 'NONE', #2628, #4723, #12763, .T. ) ;
#1786=VECTOR ( 'NONE', #402, 1000.000000000000114 ) ;
#1796=( NAMED_UNIT ( * ) SI_UNIT ( $, .STERADIAN. ) SOLID_ANGLE_UNIT ( ) );
#1835=LINE ( 'NONE', #8586, #5136 ) ;
#1885=( GEOMETRIC_REPRESENTATION_CONTEXT ( 3 ) GLOBAL_UNCERTAINTY_ASSIGNED_CONTEXT ( ( #10697 ) ) GLOBAL_UNIT_ASSIGNED_CONTEXT ( ( #659, #9826, #6700 ) ) REPRESENTATION_CONTEXT ( 'NONE', 'WORKASPACE' ) );
#1895=( GEOMETRIC_REPRESENTATION_CONTEXT ( 3 ) GLOBAL_UNCERTAINTY_ASSIGNED_CONTEXT ( ( #757 ) ) GLOBAL_UNIT_ASSIGNED_CONTEXT ( ( #6447, #10585, #1796 ) ) REPRESENTATION_CONTEXT ( 'NONE', 'WORKASPACE' ) );
#1903=CIRCLE ( 'NONE', #2841, 0.2500000000000002220 ) ;
#1946=CARTESIAN_POINT ( 'NONE',  ( -31.74999999999995737, 0.000000000000000000, 4.250000000000000000 ) ) ;
#1950=CARTESIAN_POINT ( 'NONE',  ( 0.000000000000000000, 2.357898499370431722, -2.818925648462311528E-15 ) ) ;
#1959=DIRECTION ( 'NONE',  ( 0.000000000000000000, 0.8660254037844380415, -0.5000000000000009992 ) ) ;
#1970=EDGE_CURVE ( 'NONE', #11219, #6474, #3127, .T. ) ;
#2010=FACE_OUTER_BOUND ( 'NONE', #1073, .T. ) ;
#2011=FILL_AREA_STYLE ('',( #623 ) ) ;
#2012=VECTOR ( 'NONE', #9533, 999.9999999999997726 ) ;
#2078=DIRECTION ( 'NONE',  ( -1.000000000000000000, -0.000000000000000000, -0.000000000000000000 ) ) ;
#2093=ORIENTED_EDGE ( 'NONE', *, *, #14011, .T. ) ;
#2099=FACE_OUTER_BOUND ( 'NONE', #5985, .T. ) ;
#2115=ORIENTED_EDGE ( 'NONE', *, *, #12561, .F. ) ;
#2129=MECHANICAL_DESIGN_GEOMETRIC_PRESENTATION_REPRESENTATION('',(#10937),#13699);
#2141=CARTESIAN_POINT ( 'NONE',  ( 5.000000000000000888, 0.000000000000000000, 0.000000000000000000 ) ) ;
#2153=EDGE_CURVE ( 'NONE', #4789, #11219, #8093, .T. ) ;
#2156=CARTESIAN_POINT ( 'NONE',  ( 2.500000000000000000, -2.357898499370432166, 3.035766082959412415E-15 ) ) ;
#2171=ADVANCED_FACE ( 'NONE', ( #9405 ), #8384, .F. ) ;
#2194=CARTESIAN_POINT ( 'NONE',  ( 0.2500000000000002220, 4.898587196589412829E-16, -4.000000000000000000 ) ) ;
#2213=DIRECTION ( 'NONE',  ( 1.000000000000000000, 0.000000000000000000, 0.000000000000000000 ) ) ;
#2214=ADVANCED_FACE ( 'NONE', ( #7586 ), #2290, .F. ) ;
#2218=CONICAL_SURFACE ( 'NONE', #6152, 2.055000000000000160, 0.7853981633974639331 ) ;
#2223=LINE ( 'NONE', #3397, #5479 ) ;
#2245=DIRECTION ( 'NONE',  ( 0.000000000000000000, -1.000000000000000000, 1.287488025362403787E-15 ) ) ;
#2272=CARTESIAN_POINT ( 'NONE',  ( 0.000000000000000000, 2.357898499370431722, -2.818925648462311528E-15 ) ) ;
#2280=LINE ( 'NONE', #5410, #7244 ) ;
#2290=PLANE ( 'NONE',  #2305 ) ;
#2294=CARTESIAN_POINT ( 'NONE',  ( 5.200000000000002842, 0.000000000000000000, 0.000000000000000000 ) ) ;
#2304=AXIS2_PLACEMENT_3D ( 'NONE', #2955, #6136, #748 ) ;
#2305=AXIS2_PLACEMENT_3D ( 'NONE', #7725, #2213, #12228 ) ;
#2396=ORIENTED_EDGE ( 'NONE', *, *, #6668, .F. ) ;
#2429=CARTESIAN_POINT ( 'NONE',  ( 20.55500000000001748, 0.000000000000000000, 0.000000000000000000 ) ) ;
#2439=VECTOR ( 'NONE', #5459, 1000.000000000000000 ) ;
#2456=CARTESIAN_POINT ( 'NONE',  ( 2.500000000000000000, 1.178949249685212974, -2.042000000000001148 ) ) ;
#2482=CIRCLE ( 'NONE', #2726, 0.2500000000000002220 ) ;
#2494=AXIS2_PLACEMENT_3D ( 'NONE', #6531, #10073, #104 ) ;
#2548=ORIENTED_EDGE ( 'NONE', *, *, #8156, .F. ) ;
#2581=EDGE_CURVE ( 'NONE', #4723, #6208, #8803, .T. ) ;
#2602=VERTEX_POINT ( 'NONE', #6621 ) ;
#2628=VERTEX_POINT ( 'NONE', #11474 ) ;
#2713=LINE ( 'NONE', #13796, #2012 ) ;
#2718=DIRECTION ( 'NONE',  ( 0.000000000000000000, 0.000000000000000000, -1.000000000000000000 ) ) ;
#2726=AXIS2_PLACEMENT_3D ( 'NONE', #2194, #8872, #12134 ) ;
#2730=DIRECTION ( 'NONE',  ( 1.000000000000000000, 0.000000000000000000, 0.000000000000000000 ) ) ;
#2749=CARTESIAN_POINT ( 'NONE',  ( 0.000000000000000000, 1.178949249685217415, 2.041999999999998483 ) ) ;
#2778=AXIS2_PLACEMENT_3D ( 'NONE', #2429, #10406, #435 ) ;
#2784=ORIENTED_EDGE ( 'NONE', *, *, #3663, .T. ) ;
#2796=ORIENTED_EDGE ( 'NONE', *, *, #3663, .F. ) ;
#2841=AXIS2_PLACEMENT_3D ( 'NONE', #9331, #11649, #9547 ) ;
#2852=ORIENTED_EDGE ( 'NONE', *, *, #11, .F. ) ;
#2863=ADVANCED_FACE ( 'NONE', ( #1736 ), #4146, .T. ) ;
#2884=DIRECTION ( 'NONE',  ( 0.000000000000000000, 0.000000000000000000, -1.000000000000000000 ) ) ;
#2912=ORIENTED_EDGE ( 'NONE', *, *, #12783, .T. ) ;
#2955=CARTESIAN_POINT ( 'NONE',  ( -31.74999999999995737, 0.000000000000000000, 0.000000000000000000 ) ) ;
#2976=SURFACE_SIDE_STYLE ('',( #5363 ) ) ;
#2984=ORIENTED_EDGE ( 'NONE', *, *, #7793, .F. ) ;
#2986=ORIENTED_EDGE ( 'NONE', *, *, #10743, .F. ) ;
#3007=ORIENTED_EDGE ( 'NONE', *, *, #11598, .T. ) ;
#3010=DIRECTION ( 'NONE',  ( -1.000000000000000000, -0.000000000000000000, -0.000000000000000000 ) ) ;
#3047=DIRECTION ( 'NONE',  ( 0.000000000000000000, 0.000000000000000000, -1.000000000000000000 ) ) ;
#3052=AXIS2_PLACEMENT_3D ( 'NONE', #10642, #7509, #6430 ) ;
#3060=FACE_BOUND ( 'NONE', #1002, .T. ) ;
#3066=DIRECTION ( 'NONE',  ( 0.000000000000000000, 0.000000000000000000, 1.000000000000000000 ) ) ;
#3076=EDGE_LOOP ( 'NONE', ( #10868, #5062, #7711, #8061 ) ) ;
#3093=AXIS2_PLACEMENT_3D ( 'NONE', #4314, #12078, #11207 ) ;
#3110=ORIENTED_EDGE ( 'NONE', *, *, #5180, .F. ) ;
#3127=LINE ( 'NONE', #1946, #6498 ) ;
#3129=ORIENTED_EDGE ( 'NONE', *, *, #3468, .T. ) ;
#3171=EDGE_LOOP ( 'NONE', ( #8598, #4447, #2396 ) ) ;
#3180=ORIENTED_EDGE ( 'NONE', *, *, #10216, .T. ) ;
#3182=DIRECTION ( 'NONE',  ( 0.000000000000000000, 0.000000000000000000, 1.000000000000000000 ) ) ;
#3197=VECTOR ( 'NONE', #9073, 1000.000000000000000 ) ;
#3202=DIRECTION ( 'NONE',  ( -1.000000000000000000, -0.000000000000000000, -0.000000000000000000 ) ) ;
#3257=FACE_OUTER_BOUND ( 'NONE', #12853, .T. ) ;
#3275=ORIENTED_EDGE ( 'NONE', *, *, #10475, .F. ) ;
#3281=CARTESIAN_POINT ( 'NONE',  ( 2.500000000000000000, -2.357898499370432166, 3.035766082959412415E-15 ) ) ;
#3286=EDGE_LOOP ( 'NONE', ( #5040, #123, #6490, #892 ) ) ;
#3298=AXIS2_PLACEMENT_3D ( 'NONE', #12642, #13800, #2718 ) ;
#3301=CARTESIAN_POINT ( 'NONE',  ( 2.500000000000000000, -1.178949249685214307, 2.042000000000001592 ) ) ;
#3309=EDGE_CURVE ( 'NONE', #5369, #2602, #11593, .T. ) ;
#3320=FACE_OUTER_BOUND ( 'NONE', #3286, .T. ) ;
#3322=PRODUCT_DEFINITION_FORMATION_WITH_SPECIFIED_SOURCE ( 'ANY', '', #3346, .NOT_KNOWN. ) ;
#3332=ADVANCED_FACE ( 'NONE', ( #151 ), #1384, .T. ) ;
#3345=DIRECTION ( 'NONE',  ( -1.000000000000000000, -0.000000000000000000, -0.000000000000000000 ) ) ;
#3346=PRODUCT ( 'socket head cap screw_iso_ISO 4762 M5 x 16 - 16N', 'socket head cap screw_iso_ISO 4762 M5 x 16 - 16N', '', ( #4668 ) ) ;
#3382=CARTESIAN_POINT ( 'NONE',  ( 2.500000000000000000, 2.357898499370431722, -2.818925648462311528E-15 ) ) ;
#3397=CARTESIAN_POINT ( 'NONE',  ( 0.000000000000000000, -2.357898499370432166, 3.035766082959412415E-15 ) ) ;
#3404=EDGE_CURVE ( 'NONE', #6208, #10596, #8894, .T. ) ;
#3468=EDGE_CURVE ( 'NONE', #5358, #6474, #11848, .T. ) ;
#3478=VERTEX_POINT ( 'NONE', #12722 ) ;
#3527=EDGE_CURVE ( 'NONE', #6597, #6422, #9989, .T. ) ;
#3537=LINE ( 'NONE', #7941, #3923 ) ;
#3556=FACE_OUTER_BOUND ( 'NONE', #8722, .T. ) ;
#3585=DIRECTION ( 'NONE',  ( -1.000000000000000000, -0.000000000000000000, -0.000000000000000000 ) ) ;
#3587=DIRECTION ( 'NONE',  ( -1.000000000000000000, -0.000000000000000000, -0.000000000000000000 ) ) ;
#3607=DIRECTION ( 'NONE',  ( 0.000000000000000000, 0.000000000000000000, 1.000000000000000000 ) ) ;
#3663=EDGE_CURVE ( 'NONE', #6208, #67, #1835, .T. ) ;
#3682=ORIENTED_EDGE ( 'NONE', *, *, #5797, .F. ) ;
#3683=AXIS2_PLACEMENT_3D ( 'NONE', #5870, #13766, #317 ) ;
#3687=MANIFOLD_SOLID_BREP ( 'Hex', #11696 ) ;
#3691=CARTESIAN_POINT ( 'NONE',  ( 0.000000000000000000, 0.000000000000000000, 4.000000000000000000 ) ) ;
#3739=EDGE_CURVE ( 'NONE', #12934, #6489, #13956, .T. ) ;
#3750=CARTESIAN_POINT ( 'NONE',  ( 2.500000000000000000, 2.629050547790028946E-15, 2.042000000000000259 ) ) ;
#3752=EDGE_CURVE ( 'NONE', #5974, #11887, #5463, .T. ) ;
#3769=AXIS2_PLACEMENT_3D ( 'NONE', #11136, #1178, #5619 ) ;
#3806=EDGE_CURVE ( 'NONE', #6489, #9721, #4883, .T. ) ;
#3807=ORIENTED_EDGE ( 'NONE', *, *, #3739, .T. ) ;
#3854=CARTESIAN_POINT ( 'NONE',  ( 0.000000000000000000, 1.178949249685212974, -2.042000000000001148 ) ) ;
#3865=TOROIDAL_SURFACE ( 'NONE', #349, 2.700000000000000622, 0.2000000000000000111 ) ;
#3866=EDGE_LOOP ( 'NONE', ( #8353, #118, #8905 ) ) ;
#3868=ORIENTED_EDGE ( 'NONE', *, *, #3309, .F. ) ;
#3873=AXIS2_PLACEMENT_3D ( 'NONE', #10361, #6953, #5935 ) ;
#3902=ORIENTED_EDGE ( 'NONE', *, *, #3404, .F. ) ;
#3911=PRESENTATION_STYLE_ASSIGNMENT (( #8547 ) ) ;
#3923=VECTOR ( 'NONE', #10273, 1000.000000000000000 ) ;
#3931=FACE_OUTER_BOUND ( 'NONE', #13592, .T. ) ;
#3941=ADVANCED_FACE ( 'NONE', ( #3931 ), #8488, .T. ) ;
#3951=CIRCLE ( 'NONE', #5791, 2.041999999999999815 ) ;
#4042=VERTEX_POINT ( 'NONE', #1144 ) ;
#4092=ORIENTED_EDGE ( 'NONE', *, *, #12893, .F. ) ;
#4120=EDGE_CURVE ( 'NONE', #4659, #12287, #8779, .T. ) ;
#4133=ORIENTED_EDGE ( 'NONE', *, *, #747, .T. ) ;
#4142=DIRECTION ( 'NONE',  ( -1.000000000000000000, -0.000000000000000000, -0.000000000000000000 ) ) ;
#4143=VERTEX_POINT ( 'NONE', #4722 ) ;
#4146=CYLINDRICAL_SURFACE ( 'NONE', #10866, 2.500000000000000444 ) ;
#4183=FACE_OUTER_BOUND ( 'NONE', #12513, .T. ) ;
#4204=AXIS2_PLACEMENT_3D ( 'NONE', #5982, #13801, #4833 ) ;
#4216=CARTESIAN_POINT ( 'NONE',  ( 21.00000000000000355, 0.000000000000000000, 0.000000000000000000 ) ) ;
#4245=AXIS2_PLACEMENT_3D ( 'NONE', #10708, #5203, #10555 ) ;
#4252=CARTESIAN_POINT ( 'NONE',  ( 2.500000000000000000, 1.178949249685217415, 2.041999999999998483 ) ) ;
#4267=FACE_OUTER_BOUND ( 'NONE', #3076, .T. ) ;
#4307=CARTESIAN_POINT ( 'NONE',  ( 2.500000000000000000, -1.178949249685218748, -2.041999999999998039 ) ) ;
#4314=CARTESIAN_POINT ( 'NONE',  ( 2.500000000000000000, 0.000000000000000000, 0.000000000000000000 ) ) ;
#4354=ADVANCED_FACE ( 'NONE', ( #2010 ), #13837, .F. ) ;
#4365=DIRECTION ( 'NONE',  ( -1.000000000000000000, -0.000000000000000000, -0.000000000000000000 ) ) ;
#4388=EDGE_CURVE ( 'NONE', #8912, #5974, #689, .T. ) ;
#4396=DIRECTION ( 'NONE',  ( 0.000000000000000000, 0.4999999999999990008, -0.8660254037844391517 ) ) ;
#4447=ORIENTED_EDGE ( 'NONE', *, *, #9707, .T. ) ;
#4455=CARTESIAN_POINT ( 'NONE',  ( 2.500000000000000000, -1.178949249685214307, 2.042000000000001592 ) ) ;
#4494=FACE_OUTER_BOUND ( 'NONE', #8698, .T. ) ;
#4496=ORIENTED_EDGE ( 'NONE', *, *, #7304, .F. ) ;
#4502=LINE ( 'NONE', #12180, #849 ) ;
#4621=ORIENTED_EDGE ( 'NONE', *, *, #2153, .T. ) ;
#4659=VERTEX_POINT ( 'NONE', #7076 ) ;
#4668=PRODUCT_CONTEXT ( 'NONE', #9538, 'mechanical' ) ;
#4684=DIRECTION ( 'NONE',  ( -1.000000000000000000, -0.000000000000000000, -0.000000000000000000 ) ) ;
#4716=EDGE_CURVE ( 'NONE', #12934, #9938, #3537, .T. ) ;
#4722=CARTESIAN_POINT ( 'NONE',  ( 5.200000000000002842, 3.061616997868383634E-16, -2.500000000000000444 ) ) ;
#4723=VERTEX_POINT ( 'NONE', #6863 ) ;
#4729=ADVANCED_FACE ( 'NONE', ( #1704 ), #10644, .T. ) ;
#4731=ORIENTED_EDGE ( 'NONE', *, *, #14182, .T. ) ;
#4732=LINE ( 'NONE', #10161, #3197 ) ;
#4761=DIRECTION ( 'NONE',  ( 0.000000000000000000, 0.000000000000000000, -1.000000000000000000 ) ) ;
#4789=VERTEX_POINT ( 'NONE', #8529 ) ;
#4795=ORIENTED_EDGE ( 'NONE', *, *, #3739, .F. ) ;
#4819=TOROIDAL_SURFACE ( 'NONE', #13825, 2.700000000000000622, 0.2000000000000000111 ) ;
#4833=DIRECTION ( 'NONE',  ( 0.000000000000000000, 1.224646799147353207E-16, 1.000000000000000000 ) ) ;
#4837=EDGE_CURVE ( 'NONE', #6422, #7082, #1367, .T. ) ;
#4883=LINE ( 'NONE', #3854, #12510 ) ;
#4896=CIRCLE ( 'NONE', #12079, 2.055000000000000160 ) ;
#4937=VECTOR ( 'NONE', #12137, 999.9999999999997726 ) ;
#4969=FACE_OUTER_BOUND ( 'NONE', #12928, .T. ) ;
#4988=DIRECTION ( 'NONE',  ( 0.000000000000000000, 0.000000000000000000, 1.000000000000000000 ) ) ;
#4995=ORIENTED_EDGE ( 'NONE', *, *, #4837, .T. ) ;
#5014=DIRECTION ( 'NONE',  ( 0.000000000000000000, 0.000000000000000000, 1.000000000000000000 ) ) ;
#5017=LINE ( 'NONE', #10526, #11497 ) ;
#5018=ORIENTED_EDGE ( 'NONE', *, *, #9707, .F. ) ;
#5031=ORIENTED_EDGE ( 'NONE', *, *, #6657, .F. ) ;
#5040=ORIENTED_EDGE ( 'NONE', *, *, #3468, .F. ) ;
#5051=AXIS2_PLACEMENT_3D ( 'NONE', #1730, #13989, #5014 ) ;
#5062=ORIENTED_EDGE ( 'NONE', *, *, #11598, .F. ) ;
#5077=DIRECTION ( 'NONE',  ( 1.000000000000000000, 0.000000000000000000, 0.000000000000000000 ) ) ;
#5085=AXIS2_PLACEMENT_3D ( 'NONE', #13044, #7458, #3047 ) ;
#5107=ORIENTED_EDGE ( 'NONE', *, *, #5180, .T. ) ;
#5131=VERTEX_POINT ( 'NONE', #5836 ) ;
#5136=VECTOR ( 'NONE', #13013, 1000.000000000000114 ) ;
#5149=EDGE_LOOP ( 'NONE', ( #860, #14067, #6468 ) ) ;
#5180=EDGE_CURVE ( 'NONE', #678, #2602, #8090, .T. ) ;
#5189=CARTESIAN_POINT ( 'NONE',  ( 2.500000000000000000, -1.178949249685214307, 2.042000000000001592 ) ) ;
#5203=DIRECTION ( 'NONE',  ( 0.000000000000000000, -1.000000000000000000, 0.000000000000000000 ) ) ;
#5269=LINE ( 'NONE', #10634, #6561 ) ;
#5295=CARTESIAN_POINT ( 'NONE',  ( 5.200000000000002842, 0.000000000000000000, 0.000000000000000000 ) ) ;
#5298=SHAPE_REPRESENTATION_RELATIONSHIP ( 'NONE' , 'NONE' ,  #10314, #1248 ) ;
#5358=VERTEX_POINT ( 'NONE', #734 ) ;
#5363=SURFACE_STYLE_FILL_AREA ( #2011 ) ;
#5369=VERTEX_POINT ( 'NONE', #8514 ) ;
#5393=ORIENTED_EDGE ( 'NONE', *, *, #10743, .T. ) ;
#5403=DIRECTION ( 'NONE',  ( 0.000000000000000000, -0.5000000000000009992, -0.8660254037844380415 ) ) ;
#5410=CARTESIAN_POINT ( 'NONE',  ( 2.500000000000000000, -2.357898499370432166, 3.035766082959412415E-15 ) ) ;
#5438=DIRECTION ( 'NONE',  ( 1.000000000000000000, 0.000000000000000000, 0.000000000000000000 ) ) ;
#5457=LINE ( 'NONE', #11049, #8737 ) ;
#5459=DIRECTION ( 'NONE',  ( -1.000000000000000000, -0.000000000000000000, -0.000000000000000000 ) ) ;
#5463=LINE ( 'NONE', #4455, #11819 ) ;
#5472=DIRECTION ( 'NONE',  ( 0.000000000000000000, 0.000000000000000000, -1.000000000000000000 ) ) ;
#5479=VECTOR ( 'NONE', #10258, 1000.000000000000114 ) ;
#5495=CARTESIAN_POINT ( 'NONE',  ( 2.500000000000000000, 2.357898499370431722, -2.818925648462311528E-15 ) ) ;
#5560=AXIS2_PLACEMENT_3D ( 'NONE', #14254, #2078, #3182 ) ;
#5619=DIRECTION ( 'NONE',  ( 0.000000000000000000, 0.000000000000000000, -1.000000000000000000 ) ) ;
#5622=FACE_OUTER_BOUND ( 'NONE', #813, .T. ) ;
#5683=DIRECTION ( 'NONE',  ( 0.000000000000000000, 0.5000000000000011102, 0.8660254037844379305 ) ) ;
#5692=VECTOR ( 'NONE', #11469, 1000.000000000000000 ) ;
#5759=DIRECTION ( 'NONE',  ( -1.000000000000000000, -0.000000000000000000, -0.000000000000000000 ) ) ;
#5782=AXIS2_PLACEMENT_3D ( 'NONE', #8230, #12662, #4988 ) ;
#5791=AXIS2_PLACEMENT_3D ( 'NONE', #10539, #6043, #7338 ) ;
#5797=EDGE_CURVE ( 'NONE', #1004, #8679, #8754, .T. ) ;
#5822=EDGE_LOOP ( 'NONE', ( #2796, #6073, #304 ) ) ;
#5836=CARTESIAN_POINT ( 'NONE',  ( 0.000000000000000000, -1.178949249685214307, 2.042000000000001592 ) ) ;
#5870=CARTESIAN_POINT ( 'NONE',  ( 2.500000000000000000, 0.000000000000000000, 0.000000000000000000 ) ) ;
#5912=DIRECTION ( 'NONE',  ( 0.000000000000000000, 0.000000000000000000, 1.000000000000000000 ) ) ;
#5935=DIRECTION ( 'NONE',  ( 0.000000000000000000, 0.000000000000000000, 1.000000000000000000 ) ) ;
#5970=ORIENTED_EDGE ( 'NONE', *, *, #14031, .T. ) ;
#5974=VERTEX_POINT ( 'NONE', #3750 ) ;
#5982=CARTESIAN_POINT ( 'NONE',  ( 5.200000000000002842, 3.306546357697854226E-16, 2.700000000000000622 ) ) ;
#5985=EDGE_LOOP ( 'NONE', ( #12016, #13048 ) ) ;
#6021=CARTESIAN_POINT ( 'NONE',  ( 2.500000000000000000, 2.500728763858895382E-16, -2.041999999999999815 ) ) ;
#6043=DIRECTION ( 'NONE',  ( -1.000000000000000000, -0.000000000000000000, -0.000000000000000000 ) ) ;
#6047=DIRECTION ( 'NONE',  ( 0.000000000000000000, 0.000000000000000000, 1.000000000000000000 ) ) ;
#6051=CARTESIAN_POINT ( 'NONE',  ( 2.500000000000000000, 1.178949249685212974, -2.042000000000001148 ) ) ;
#6058=ORIENTED_EDGE ( 'NONE', *, *, #8926, .T. ) ;
#6073=ORIENTED_EDGE ( 'NONE', *, *, #2581, .F. ) ;
#6076=CARTESIAN_POINT ( 'NONE',  ( 0.2500000000000002220, 0.000000000000000000, 0.000000000000000000 ) ) ;
#6101=CYLINDRICAL_SURFACE ( 'NONE', #13601, 4.250000000000000000 ) ;
#6133=CARTESIAN_POINT ( 'NONE',  ( 5.200000000000002842, 0.000000000000000000, 0.000000000000000000 ) ) ;
#6136=DIRECTION ( 'NONE',  ( -1.000000000000000000, -0.000000000000000000, -0.000000000000000000 ) ) ;
#6152=AXIS2_PLACEMENT_3D ( 'NONE', #172, #3345, #3607 ) ;
#6153=DIRECTION ( 'NONE',  ( -0.7071067811865364705, 8.659560562355067211E-17, -0.7071067811865584529 ) ) ;
#6208=VERTEX_POINT ( 'NONE', #3281 ) ;
#6244=ORIENTED_EDGE ( 'NONE', *, *, #977, .T. ) ;
#6268=AXIS2_PLACEMENT_3D ( 'NONE', #11143, #4684, #12148 ) ;
#6298=( NAMED_UNIT ( * ) PLANE_ANGLE_UNIT ( ) SI_UNIT ( $, .RADIAN. ) );
#6299=AXIS2_PLACEMENT_3D ( 'NONE', #11793, #2730, #13963 ) ;
#6330=ADVANCED_FACE ( 'NONE', ( #3556 ), #7336, .F. ) ;
#6333=CIRCLE ( 'NONE', #12340, 2.700000000000000622 ) ;
#6369=ADVANCED_FACE ( 'NONE', ( #1434 ), #1644, .T. ) ;
#6373=( LENGTH_UNIT ( ) NAMED_UNIT ( * ) SI_UNIT ( .MILLI., .METRE. ) );
#6384=EDGE_LOOP ( 'NONE', ( #9160, #14001 ) ) ;
#6392=DIRECTION ( 'NONE',  ( 0.000000000000000000, 0.5000000000000009992, 0.8660254037844380415 ) ) ;
#6408=CARTESIAN_POINT ( 'NONE',  ( -31.74999999999995737, 3.061616997868383634E-16, -2.500000000000000444 ) ) ;
#6422=VERTEX_POINT ( 'NONE', #8067 ) ;
#6430=DIRECTION ( 'NONE',  ( 0.000000000000000000, 1.000000000000000000, -1.287488025362403787E-15 ) ) ;
#6440=ADVANCED_FACE ( 'NONE', ( #1322 ), #71, .T. ) ;
#6447=( LENGTH_UNIT ( ) NAMED_UNIT ( * ) SI_UNIT ( .MILLI., .METRE. ) );
#6463=ADVANCED_FACE ( 'NONE', ( #10320 ), #9098, .F. ) ;
#6468=ORIENTED_EDGE ( 'NONE', *, *, #1262, .F. ) ;
#6474=VERTEX_POINT ( 'NONE', #12501 ) ;
#6489=VERTEX_POINT ( 'NONE', #7780 ) ;
#6490=ORIENTED_EDGE ( 'NONE', *, *, #977, .F. ) ;
#6498=VECTOR ( 'NONE', #3202, 1000.000000000000000 ) ;
#6529=DIRECTION ( 'NONE',  ( 0.000000000000000000, 0.000000000000000000, -1.000000000000000000 ) ) ;
#6531=CARTESIAN_POINT ( 'NONE',  ( 2.500000000000000000, 0.000000000000000000, 0.000000000000000000 ) ) ;
#6546=CARTESIAN_POINT ( 'NONE',  ( 0.000000000000000000, 0.000000000000000000, 0.000000000000000000 ) ) ;
#6561=VECTOR ( 'NONE', #666, 1000.000000000000000 ) ;
#6563=ORIENTED_EDGE ( 'NONE', *, *, #1970, .T. ) ;
#6570=DIRECTION ( 'NONE',  ( -1.000000000000000000, -0.000000000000000000, -0.000000000000000000 ) ) ;
#6582=DIRECTION ( 'NONE',  ( -0.000000000000000000, 0.8660254037844392627, 0.4999999999999990008 ) ) ;
#6597=VERTEX_POINT ( 'NONE', #11703 ) ;
#6613=DIRECTION ( 'NONE',  ( -1.000000000000000000, 0.000000000000000000, -0.000000000000000000 ) ) ;
#6621=CARTESIAN_POINT ( 'NONE',  ( 20.55500000000001748, 3.061616997868384127E-16, -2.500000000000000888 ) ) ;
#6655=AXIS2_PLACEMENT_3D ( 'NONE', #4216, #4142, #8635 ) ;
#6657=EDGE_CURVE ( 'NONE', #12287, #9466, #2713, .T. ) ;
#6668=EDGE_CURVE ( 'NONE', #4723, #5974, #10122, .T. ) ;
#6676=CIRCLE ( 'NONE', #152, 2.041999999999999815 ) ;
#6686=ORIENTED_EDGE ( 'NONE', *, *, #13377, .T. ) ;
#6687=FACE_BOUND ( 'NONE', #12851, .T. ) ;
#6700=( NAMED_UNIT ( * ) SI_UNIT ( $, .STERADIAN. ) SOLID_ANGLE_UNIT ( ) );
#6718=DIRECTION ( 'NONE',  ( 1.000000000000000000, 0.000000000000000000, 0.000000000000000000 ) ) ;
#6824=LINE ( 'NONE', #6021, #1786 ) ;
#6863=CARTESIAN_POINT ( 'NONE',  ( 2.500000000000000000, -1.768423874527823569, 1.021000000000002350 ) ) ;
#6881=DIRECTION ( 'NONE',  ( 0.000000000000000000, -1.000000000000000000, 1.287488025362403787E-15 ) ) ;
#6889=EDGE_CURVE ( 'NONE', #9466, #6489, #795, .T. ) ;
#6898=ORIENTED_EDGE ( 'NONE', *, *, #11104, .T. ) ;
#6946=ORIENTED_EDGE ( 'NONE', *, *, #10540, .T. ) ;
#6953=DIRECTION ( 'NONE',  ( -1.000000000000000000, -0.000000000000000000, -0.000000000000000000 ) ) ;
#7027=EDGE_CURVE ( 'NONE', #5131, #9938, #635, .T. ) ;
#7033=ORIENTED_EDGE ( 'NONE', *, *, #10587, .F. ) ;
#7043=PLANE ( 'NONE',  #11068 ) ;
#7076=CARTESIAN_POINT ( 'NONE',  ( 2.500000000000000000, 1.768423874527823791, 1.020999999999998353 ) ) ;
#7082=VERTEX_POINT ( 'NONE', #7109 ) ;
#7091=DIRECTION ( 'NONE',  ( 0.000000000000000000, -0.8660254037844390407, -0.4999999999999993339 ) ) ;
#7109=CARTESIAN_POINT ( 'NONE',  ( 5.000000000000002665, 0.000000000000000000, -2.700000000000000622 ) ) ;
#7200=AXIS2_PLACEMENT_3D ( 'NONE', #2156, #6582, #11008 ) ;
#7207=ADVANCED_FACE ( 'NONE', ( #3060, #2099 ), #9586, .T. ) ;
#7217=FACE_OUTER_BOUND ( 'NONE', #3866, .T. ) ;
#7244=VECTOR ( 'NONE', #4396, 1000.000000000000114 ) ;
#7281=EDGE_LOOP ( 'NONE', ( #6244, #7555 ) ) ;
#7304=EDGE_CURVE ( 'NONE', #11887, #9938, #1211, .T. ) ;
#7336=CONICAL_SURFACE ( 'NONE', #3873, 2.041999999999999815, 1.047197551196591858 ) ;
#7338=DIRECTION ( 'NONE',  ( 0.000000000000000000, 0.000000000000000000, 1.000000000000000000 ) ) ;
#7347=CARTESIAN_POINT ( 'NONE',  ( 2.500000000000000000, -1.178949249685218748, -2.041999999999998039 ) ) ;
#7349=LINE ( 'NONE', #5189, #12316 ) ;
#7355=ORIENTED_EDGE ( 'NONE', *, *, #6668, .T. ) ;
#7421=ORIENTED_EDGE ( 'NONE', *, *, #1636, .F. ) ;
#7458=DIRECTION ( 'NONE',  ( 1.000000000000000000, 0.000000000000000000, 0.000000000000000000 ) ) ;
#7509=DIRECTION ( 'NONE',  ( 0.000000000000000000, -1.287488025362403787E-15, -1.000000000000000000 ) ) ;
#7512=DIRECTION ( 'NONE',  ( 0.000000000000000000, 0.000000000000000000, -1.000000000000000000 ) ) ;
#7555=ORIENTED_EDGE ( 'NONE', *, *, #5797, .T. ) ;
#7586=FACE_OUTER_BOUND ( 'NONE', #3171, .T. ) ;
#7611=CARTESIAN_POINT ( 'NONE',  ( 0.2500000000000002220, 0.000000000000000000, 0.000000000000000000 ) ) ;
#7659=AXIS2_PLACEMENT_3D ( 'NONE', #10478, #12643, #12508 ) ;
#7669=CARTESIAN_POINT ( 'NONE',  ( 20.55500000000001748, 0.000000000000000000, 2.500000000000000888 ) ) ;
#7711=ORIENTED_EDGE ( 'NONE', *, *, #10587, .T. ) ;
#7721=CARTESIAN_POINT ( 'NONE',  ( 0.2500000000000002220, 0.000000000000000000, 0.000000000000000000 ) ) ;
#7725=CARTESIAN_POINT ( 'NONE',  ( 2.500000000000000000, 2.357898499370431722, -2.818925648462311528E-15 ) ) ;
#7727=ADVANCED_FACE ( 'NONE', ( #4267 ), #3865, .F. ) ;
#7780=CARTESIAN_POINT ( 'NONE',  ( 0.000000000000000000, 1.178949249685212974, -2.042000000000001148 ) ) ;
#7783=ORIENTED_EDGE ( 'NONE', *, *, #8134, .T. ) ;
#7793=EDGE_CURVE ( 'NONE', #10596, #9721, #2223, .T. ) ;
#7794=AXIS2_PLACEMENT_3D ( 'NONE', #3382, #12217, #5683 ) ;
#7796=VECTOR ( 'NONE', #14230, 1000.000000000000000 ) ;
#7866=AXIS2_PLACEMENT_3D ( 'NONE', #11912, #1959, #6392 ) ;
#7872=CIRCLE ( 'NONE', #7907, 4.250000000000000000 ) ;
#7902=VERTEX_POINT ( 'NONE', #7347 ) ;
#7907=AXIS2_PLACEMENT_3D ( 'NONE', #6076, #12533, #13898 ) ;
#7941=CARTESIAN_POINT ( 'NONE',  ( 0.000000000000000000, 2.357898499370431722, -2.818925648462311528E-15 ) ) ;
#7951=CARTESIAN_POINT ( 'NONE',  ( 2.500000000000000000, 1.178949249685217415, 2.041999999999998483 ) ) ;
#7972=DIRECTION ( 'NONE',  ( 0.000000000000000000, 0.000000000000000000, -1.000000000000000000 ) ) ;
#8042=AXIS2_PLACEMENT_3D ( 'NONE', #11841, #13932, #8418 ) ;
#8056=SHAPE_DEFINITION_REPRESENTATION ( #8076, #10314 ) ;
#8058=ORIENTED_EDGE ( 'NONE', *, *, #11290, .T. ) ;
#8061=ORIENTED_EDGE ( 'NONE', *, *, #4837, .F. ) ;
#8067=CARTESIAN_POINT ( 'NONE',  ( 5.000000000000002665, 3.306546357697854226E-16, 2.700000000000000622 ) ) ;
#8076=PRODUCT_DEFINITION_SHAPE ( 'NONE', 'NONE',  #8892 ) ;
#8090=CIRCLE ( 'NONE', #2778, 2.500000000000000888 ) ;
#8093=CIRCLE ( 'NONE', #5782, 4.250000000000000000 ) ;
#8116=LINE ( 'NONE', #11324, #28 ) ;
#8126=DIRECTION ( 'NONE',  ( 0.000000000000000000, -1.000000000000000000, 1.287488025362403787E-15 ) ) ;
#8134=EDGE_CURVE ( 'NONE', #7902, #9721, #14305, .T. ) ;
#8156=EDGE_CURVE ( 'NONE', #5131, #10596, #11932, .T. ) ;
#8205=EDGE_LOOP ( 'NONE', ( #11310, #13599, #3275, #7033 ) ) ;
#8212=PLANE ( 'NONE',  #3298 ) ;
#8230=CARTESIAN_POINT ( 'NONE',  ( 4.999999999999997335, 0.000000000000000000, 0.000000000000000000 ) ) ;
#8352=ORIENTED_EDGE ( 'NONE', *, *, #11, .T. ) ;
#8353=ORIENTED_EDGE ( 'NONE', *, *, #3752, .T. ) ;
#8384=PLANE ( 'NONE',  #199 ) ;
#8394=CARTESIAN_POINT ( 'NONE',  ( 21.00000000000000355, 2.516649172247811061E-16, -2.055000000000000160 ) ) ;
#8418=DIRECTION ( 'NONE',  ( 0.000000000000000000, 0.000000000000000000, 1.000000000000000000 ) ) ;
#8428=DIRECTION ( 'NONE',  ( -1.000000000000000000, -0.000000000000000000, -0.000000000000000000 ) ) ;
#8432=FACE_OUTER_BOUND ( 'NONE', #10162, .T. ) ;
#8452=DIRECTION ( 'NONE',  ( -1.000000000000000000, -0.000000000000000000, -0.000000000000000000 ) ) ;
#8472=AXIS2_PLACEMENT_3D ( 'NONE', #848, #5438, #6529 ) ;
#8481=DIRECTION ( 'NONE',  ( 0.000000000000000000, 0.000000000000000000, 1.000000000000000000 ) ) ;
#8488=PLANE ( 'NONE',  #7866 ) ;
#8490=AXIS2_PLACEMENT_3D ( 'NONE', #13165, #11209, #9020 ) ;
#8503=ORIENTED_EDGE ( 'NONE', *, *, #4388, .F. ) ;
#8514=CARTESIAN_POINT ( 'NONE',  ( 21.00000000000000355, 2.789133085058097101E-16, -2.055000000000000160 ) ) ;
#8529=CARTESIAN_POINT ( 'NONE',  ( 4.999999999999997335, 5.204748896376250699E-16, -4.250000000000000000 ) ) ;
#8532=EDGE_CURVE ( 'NONE', #4042, #7902, #4502, .T. ) ;
#8547=SURFACE_STYLE_USAGE ( .BOTH. , #2976 ) ;
#8561=DIRECTION ( 'NONE',  ( -1.000000000000000000, -0.000000000000000000, -0.000000000000000000 ) ) ;
#8566=DIRECTION ( 'NONE',  ( -1.000000000000000000, -0.000000000000000000, -0.000000000000000000 ) ) ;
#8586=CARTESIAN_POINT ( 'NONE',  ( 2.500000000000000000, -2.357898499370432166, 3.035766082959412415E-15 ) ) ;
#8598=ORIENTED_EDGE ( 'NONE', *, *, #1761, .F. ) ;
#8600=PLANE ( 'NONE',  #3052 ) ;
#8635=DIRECTION ( 'NONE',  ( 0.000000000000000000, 0.000000000000000000, 1.000000000000000000 ) ) ;
#8662=ORIENTED_EDGE ( 'NONE', *, *, #8532, .F. ) ;
#8676=DIRECTION ( 'NONE',  ( 1.000000000000000000, 0.000000000000000000, 0.000000000000000000 ) ) ;
#8679=VERTEX_POINT ( 'NONE', #3691 ) ;
#8698=EDGE_LOOP ( 'NONE', ( #1577, #9035, #3110, #2115 ) ) ;
#8722=EDGE_LOOP ( 'NONE', ( #8503, #2912, #309, #4731, #7355 ) ) ;
#8737=VECTOR ( 'NONE', #13218, 1000.000000000000114 ) ;
#8754=CIRCLE ( 'NONE', #8042, 4.000000000000000000 ) ;
#8776=VECTOR ( 'NONE', #5403, 1000.000000000000114 ) ;
#8779=CIRCLE ( 'NONE', #3683, 2.041999999999999815 ) ;
#8781=CARTESIAN_POINT ( 'NONE',  ( 0.000000000000000000, -1.178949249685218748, -2.041999999999998039 ) ) ;
#8803=LINE ( 'NONE', #3301, #8776 ) ;
#8872=DIRECTION ( 'NONE',  ( -0.000000000000000000, 1.000000000000000000, 1.224646799147353207E-16 ) ) ;
#8892=PRODUCT_DEFINITION ( 'UNKNOWN', '', #3322, #13781 ) ;
#8894=LINE ( 'NONE', #13306, #1175 ) ;
#8905=ORIENTED_EDGE ( 'NONE', *, *, #13377, .F. ) ;
#8912=VERTEX_POINT ( 'NONE', #12162 ) ;
#8926=EDGE_CURVE ( 'NONE', #3478, #12934, #10130, .T. ) ;
#8934=FACE_OUTER_BOUND ( 'NONE', #7281, .T. ) ;
#9011=DIRECTION ( 'NONE',  ( 0.000000000000000000, 1.000000000000000000, -1.287488025362403787E-15 ) ) ;
#9020=DIRECTION ( 'NONE',  ( 0.000000000000000000, -1.000000000000000000, 1.287488025362403787E-15 ) ) ;
#9030=CIRCLE ( 'NONE', #5560, 4.000000000000000000 ) ;
#9035=ORIENTED_EDGE ( 'NONE', *, *, #3309, .T. ) ;
#9064=TOROIDAL_SURFACE ( 'NONE', #9771, 4.000000000000000000, 0.2500000000000000000 ) ;
#9073=DIRECTION ( 'NONE',  ( -1.000000000000000000, -0.000000000000000000, -0.000000000000000000 ) ) ;
#9098=PLANE ( 'NONE',  #7794 ) ;
#9117=EDGE_LOOP ( 'NONE', ( #3868, #2093, #11676, #2852 ) ) ;
#9124=ORIENTED_EDGE ( 'NONE', *, *, #12783, .F. ) ;
#9160=ORIENTED_EDGE ( 'NONE', *, *, #11810, .F. ) ;
#9210=ORIENTED_EDGE ( 'NONE', *, *, #7793, .T. ) ;
#9221=FACE_OUTER_BOUND ( 'NONE', #5822, .T. ) ;
#9255=ADVANCED_FACE ( 'NONE', ( #4183 ), #8600, .F. ) ;
#9291=DIRECTION ( 'NONE',  ( 0.000000000000000000, -0.5000000000000009992, -0.8660254037844380415 ) ) ;
#9312=CARTESIAN_POINT ( 'NONE',  ( 2.500000000000000000, 1.768423874527822459, -1.021000000000002794 ) ) ;
#9329=DIRECTION ( 'NONE',  ( -1.000000000000000000, -0.000000000000000000, -0.000000000000000000 ) ) ;
#9331=CARTESIAN_POINT ( 'NONE',  ( 0.2500000000000002220, 0.000000000000000000, 4.000000000000000000 ) ) ;
#9333=CONICAL_SURFACE ( 'NONE', #3093, 2.041999999999999815, 1.047197551196591858 ) ;
#9405=FACE_OUTER_BOUND ( 'NONE', #5149, .T. ) ;
#9406=ADVANCED_FACE ( 'NONE', ( #3320 ), #9064, .T. ) ;
#9418=DIRECTION ( 'NONE',  ( 0.000000000000000000, 0.000000000000000000, 1.000000000000000000 ) ) ;
#9453=DIRECTION ( 'NONE',  ( -1.000000000000000000, -0.000000000000000000, -0.000000000000000000 ) ) ;
#9466=VERTEX_POINT ( 'NONE', #6051 ) ;
#9502=ADVANCED_FACE ( 'NONE', ( #4969 ), #8212, .F. ) ;
#9533=DIRECTION ( 'NONE',  ( 0.000000000000000000, -0.5000000000000013323, -0.8660254037844380415 ) ) ;
#9538=APPLICATION_CONTEXT ( 'automotive_design' ) ;
#9547=DIRECTION ( 'NONE',  ( 0.000000000000000000, 0.000000000000000000, -1.000000000000000000 ) ) ;
#9580=ORIENTED_EDGE ( 'NONE', *, *, #4716, .F. ) ;
#9586=PLANE ( 'NONE',  #8472 ) ;
#9597=EDGE_LOOP ( 'NONE', ( #215, #4621, #6563, #8058 ) ) ;
#9684=ADVANCED_FACE ( 'NONE', ( #8432 ), #11863, .T. ) ;
#9707=EDGE_CURVE ( 'NONE', #2628, #5974, #7349, .T. ) ;
#9713=DIRECTION ( 'NONE',  ( 1.000000000000000000, 0.000000000000000000, 0.000000000000000000 ) ) ;
#9721=VERTEX_POINT ( 'NONE', #8781 ) ;
#9758=VECTOR ( 'NONE', #6153, 1000.000000000000114 ) ;
#9763=AXIS2_PLACEMENT_3D ( 'NONE', #2294, #6718, #12158 ) ;
#9771=AXIS2_PLACEMENT_3D ( 'NONE', #7721, #1104, #13305 ) ;
#9777=EDGE_CURVE ( 'NONE', #9466, #4042, #1359, .T. ) ;
#9797=LINE ( 'NONE', #14202, #10203 ) ;
#9826=( NAMED_UNIT ( * ) PLANE_ANGLE_UNIT ( ) SI_UNIT ( $, .RADIAN. ) );
#9831=ORIENTED_EDGE ( 'NONE', *, *, #4716, .T. ) ;
#9896=AXIS2_PLACEMENT_3D ( 'NONE', #1249, #3587, #147 ) ;
#9907=DIRECTION ( 'NONE',  ( 0.000000000000000000, 0.000000000000000000, 1.000000000000000000 ) ) ;
#9938=VERTEX_POINT ( 'NONE', #2749 ) ;
#9989=CIRCLE ( 'NONE', #4204, 0.2000000000000000944 ) ;
#10003=DIRECTION ( 'NONE',  ( 0.000000000000000000, 0.000000000000000000, 1.000000000000000000 ) ) ;
#10045=FACE_OUTER_BOUND ( 'NONE', #12941, .T. ) ;
#10051=CARTESIAN_POINT ( 'NONE',  ( 2.500000000000000000, 0.000000000000000000, 0.000000000000000000 ) ) ;
#10073=DIRECTION ( 'NONE',  ( -1.000000000000000000, -0.000000000000000000, -0.000000000000000000 ) ) ;
#10121=EDGE_LOOP ( 'NONE', ( #9580, #13145, #6898, #5970, #12932 ) ) ;
#10122=CIRCLE ( 'NONE', #1311, 2.041999999999999815 ) ;
#10125=CARTESIAN_POINT ( 'NONE',  ( 5.200000000000002842, 0.000000000000000000, 0.000000000000000000 ) ) ;
#10130=LINE ( 'NONE', #5495, #12656 ) ;
#10143=EDGE_CURVE ( 'NONE', #6597, #4143, #14174, .T. ) ;
#10160=ORIENTED_EDGE ( 'NONE', *, *, #3806, .F. ) ;
#10161=CARTESIAN_POINT ( 'NONE',  ( -31.74999999999995737, 5.204748896376250699E-16, -4.250000000000000000 ) ) ;
#10162=EDGE_LOOP ( 'NONE', ( #17, #11377, #3180, #3682 ) ) ;
#10203=VECTOR ( 'NONE', #13113, 1000.000000000000000 ) ;
#10207=STYLED_ITEM('',(#14417),#3687);
#10216=EDGE_CURVE ( 'NONE', #6474, #8679, #1903, .T. ) ;
#10238=VECTOR ( 'NONE', #6881, 1000.000000000000000 ) ;
#10249=ADVANCED_FACE ( 'NONE', ( #7217 ), #12810, .F. ) ;
#10258=DIRECTION ( 'NONE',  ( 0.000000000000000000, 0.4999999999999990008, -0.8660254037844391517 ) ) ;
#10273=DIRECTION ( 'NONE',  ( 0.000000000000000000, -0.4999999999999993339, 0.8660254037844390407 ) ) ;
#10277=CARTESIAN_POINT ( 'NONE',  ( 4.999999999999997335, 0.000000000000000000, 0.000000000000000000 ) ) ;
#10314=SHAPE_REPRESENTATION ( 'socket head cap screw_iso_ISO 4762 M5 x 16 - 16N', ( #14039 ), #1895 ) ;
#10320=FACE_OUTER_BOUND ( 'NONE', #14289, .T. ) ;
#10361=CARTESIAN_POINT ( 'NONE',  ( 2.500000000000000000, 0.000000000000000000, 0.000000000000000000 ) ) ;
#10377=CARTESIAN_POINT ( 'NONE',  ( 0.000000000000000000, -1.178949249685214307, 2.042000000000001592 ) ) ;
#10406=DIRECTION ( 'NONE',  ( -1.000000000000000000, -0.000000000000000000, -0.000000000000000000 ) ) ;
#10449=EDGE_LOOP ( 'NONE', ( #5107, #10779, #3007, #10759 ) ) ;
#10475=EDGE_CURVE ( 'NONE', #7082, #6422, #6333, .T. ) ;
#10478=CARTESIAN_POINT ( 'NONE',  ( 0.2500000000000002220, 0.000000000000000000, 0.000000000000000000 ) ) ;
#10485=AXIS2_PLACEMENT_3D ( 'NONE', #6546, #6613, #12193 ) ;
#10508=CARTESIAN_POINT ( 'NONE',  ( 0.000000000000000000, 0.000000000000000000, 0.000000000000000000 ) ) ;
#10520=CARTESIAN_POINT ( 'NONE',  ( 2.500000000000000000, -1.178949249685214307, 2.042000000000001592 ) ) ;
#10526=CARTESIAN_POINT ( 'NONE',  ( 2.500000000000000000, 2.357898499370431722, -2.818925648462311528E-15 ) ) ;
#10539=CARTESIAN_POINT ( 'NONE',  ( 2.500000000000000000, 0.000000000000000000, 0.000000000000000000 ) ) ;
#10540=EDGE_CURVE ( 'NONE', #678, #6597, #5269, .T. ) ;
#10555=DIRECTION ( 'NONE',  ( 0.000000000000000000, 0.000000000000000000, -1.000000000000000000 ) ) ;
#10585=( NAMED_UNIT ( * ) PLANE_ANGLE_UNIT ( ) SI_UNIT ( $, .RADIAN. ) );
#10587=EDGE_CURVE ( 'NONE', #4143, #7082, #43, .T. ) ;
#10596=VERTEX_POINT ( 'NONE', #588 ) ;
#10618=EDGE_LOOP ( 'NONE', ( #1083, #8352, #6946, #10667 ) ) ;
#10625=CARTESIAN_POINT ( 'NONE',  ( 2.500000000000000000, 0.000000000000000000, 0.000000000000000000 ) ) ;
#10634=CARTESIAN_POINT ( 'NONE',  ( -31.74999999999995737, 0.000000000000000000, 2.500000000000000444 ) ) ;
#10642=CARTESIAN_POINT ( 'NONE',  ( 2.500000000000000000, 1.178949249685212974, -2.042000000000001148 ) ) ;
#10644=CYLINDRICAL_SURFACE ( 'NONE', #2304, 4.250000000000000000 ) ;
#10667=ORIENTED_EDGE ( 'NONE', *, *, #10143, .T. ) ;
#10697=UNCERTAINTY_MEASURE_WITH_UNIT (LENGTH_MEASURE( 1.000000000000000082E-05 ), #659, 'distance_accuracy_value', 'NONE');
#10700=DIRECTION ( 'NONE',  ( 0.000000000000000000, 0.000000000000000000, 1.000000000000000000 ) ) ;
#10708=CARTESIAN_POINT ( 'NONE',  ( 5.200000000000002842, 0.000000000000000000, -2.700000000000000622 ) ) ;
#10727=AXIS2_PLACEMENT_3D ( 'NONE', #10125, #12516, #4761 ) ;
#10743=EDGE_CURVE ( 'NONE', #67, #7902, #2280, .T. ) ;
#10758=ORIENTED_EDGE ( 'NONE', *, *, #3404, .T. ) ;
#10759=ORIENTED_EDGE ( 'NONE', *, *, #10540, .F. ) ;
#10773=ADVANCED_FACE ( 'NONE', ( #12212 ), #13364, .T. ) ;
#10776=CIRCLE ( 'NONE', #1019, 2.500000000000000888 ) ;
#10778=ADVANCED_FACE ( 'NONE', ( #10045 ), #9333, .F. ) ;
#10779=ORIENTED_EDGE ( 'NONE', *, *, #13637, .T. ) ;
#10789=CARTESIAN_POINT ( 'NONE',  ( 5.000000000000000888, 0.000000000000000000, 0.000000000000000000 ) ) ;
#10818=ORIENTED_EDGE ( 'NONE', *, *, #1970, .F. ) ;
#10821=CARTESIAN_POINT ( 'NONE',  ( -31.74999999999995737, 0.000000000000000000, 0.000000000000000000 ) ) ;
#10866=AXIS2_PLACEMENT_3D ( 'NONE', #10821, #8566, #3066 ) ;
#10868=ORIENTED_EDGE ( 'NONE', *, *, #3527, .F. ) ;
#10899=ORIENTED_EDGE ( 'NONE', *, *, #1262, .T. ) ;
#10937=STYLED_ITEM ( 'NONE', ( #3911 ), #1248 ) ;
#11008=DIRECTION ( 'NONE',  ( 0.000000000000000000, -0.4999999999999989453, 0.8660254037844391517 ) ) ;
#11024=CIRCLE ( 'NONE', #12870, 4.250000000000000000 ) ;
#11047=PLANE ( 'NONE',  #10485 ) ;
#11049=CARTESIAN_POINT ( 'NONE',  ( 21.00000000000000355, 0.000000000000000000, 2.055000000000000160 ) ) ;
#11064=VECTOR ( 'NONE', #13077, 1000.000000000000114 ) ;
#11068=AXIS2_PLACEMENT_3D ( 'NONE', #11470, #11331, #7972 ) ;
#11074=ORIENTED_EDGE ( 'NONE', *, *, #3752, .F. ) ;
#11104=EDGE_CURVE ( 'NONE', #3478, #4659, #9797, .T. ) ;
#11136=CARTESIAN_POINT ( 'NONE',  ( 21.00000000000000000, 2.055000000000000160, 0.000000000000000000 ) ) ;
#11143=CARTESIAN_POINT ( 'NONE',  ( 21.00000000000000355, 0.000000000000000000, 0.000000000000000000 ) ) ;
#11168=DIRECTION ( 'NONE',  ( -1.000000000000000000, -0.000000000000000000, -0.000000000000000000 ) ) ;
#11207=DIRECTION ( 'NONE',  ( 0.000000000000000000, 0.000000000000000000, 1.000000000000000000 ) ) ;
#11209=DIRECTION ( 'NONE',  ( -0.000000000000000000, 1.287488025362403787E-15, 1.000000000000000000 ) ) ;
#11219=VERTEX_POINT ( 'NONE', #99 ) ;
#11250=DIRECTION ( 'NONE',  ( 0.000000000000000000, -0.5000000000000013323, -0.8660254037844380415 ) ) ;
#11290=EDGE_CURVE ( 'NONE', #6474, #5358, #7872, .T. ) ;
#11310=ORIENTED_EDGE ( 'NONE', *, *, #10143, .F. ) ;
#11324=CARTESIAN_POINT ( 'NONE',  ( 2.500000000000000000, 2.357898499370431722, -2.818925648462311528E-15 ) ) ;
#11331=DIRECTION ( 'NONE',  ( 1.000000000000000000, 0.000000000000000000, 0.000000000000000000 ) ) ;
#11377=ORIENTED_EDGE ( 'NONE', *, *, #11290, .F. ) ;
#11430=ORIENTED_EDGE ( 'NONE', *, *, #6889, .T. ) ;
#11452=CARTESIAN_POINT ( 'NONE',  ( 2.500000000000000000, 2.357898499370431722, -2.818925648462311528E-15 ) ) ;
#11469=DIRECTION ( 'NONE',  ( 0.000000000000000000, 1.000000000000000000, -1.287488025362403787E-15 ) ) ;
#11470=CARTESIAN_POINT ( 'NONE',  ( 2.500000000000000000, 2.357898499370431722, -2.818925648462311528E-15 ) ) ;
#11474=CARTESIAN_POINT ( 'NONE',  ( 2.500000000000000000, -1.178949249685214307, 2.042000000000001592 ) ) ;
#11497=VECTOR ( 'NONE', #13923, 1000.000000000000000 ) ;
#11501=DIRECTION ( 'NONE',  ( 0.000000000000000000, 0.000000000000000000, -1.000000000000000000 ) ) ;
#11525=DIRECTION ( 'NONE',  ( 0.000000000000000000, 0.4999999999999992784, -0.8660254037844389297 ) ) ;
#11593=LINE ( 'NONE', #8394, #9758 ) ;
#11598=EDGE_CURVE ( 'NONE', #4143, #6597, #686, .T. ) ;
#11613=UNCERTAINTY_MEASURE_WITH_UNIT (LENGTH_MEASURE( 1.000000000000000082E-05 ), #6373, 'distance_accuracy_value', 'NONE');
#11624=CARTESIAN_POINT ( 'NONE',  ( 20.55500000000001748, 0.000000000000000000, 0.000000000000000000 ) ) ;
#11630=CARTESIAN_POINT ( 'NONE',  ( 21.00000000000000355, 0.000000000000000000, 2.055000000000000160 ) ) ;
#11649=DIRECTION ( 'NONE',  ( 0.000000000000000000, -1.000000000000000000, 0.000000000000000000 ) ) ;
#11667=ADVANCED_FACE ( 'NONE', ( #3257 ), #12095, .T. ) ;
#11676=ORIENTED_EDGE ( 'NONE', *, *, #12561, .T. ) ;
#11696=CLOSED_SHELL ( 'NONE', ( #6330, #9406, #13099, #711, #2863, #14028, #1401, #4729, #7207, #6440, #3332, #10773, #7727, #9684, #6369, #12077, #3941, #11667, #9255, #6463, #9502, #13917, #2214, #10249, #4354, #2171, #10778 ) ) ;
#11703=CARTESIAN_POINT ( 'NONE',  ( 5.200000000000002842, 0.000000000000000000, 2.500000000000000444 ) ) ;
#11738=DIRECTION ( 'NONE',  ( 0.000000000000000000, 0.000000000000000000, -1.000000000000000000 ) ) ;
#11739=VECTOR ( 'NONE', #3585, 1000.000000000000000 ) ;
#11750=CIRCLE ( 'NONE', #6655, 2.055000000000000160 ) ;
#11767=CIRCLE ( 'NONE', #2494, 2.041999999999999815 ) ;
#11787=AXIS2_PLACEMENT_3D ( 'NONE', #10789, #8452, #2884 ) ;
#11793=CARTESIAN_POINT ( 'NONE',  ( 2.500000000000000000, 2.357898499370431722, -2.818925648462311528E-15 ) ) ;
#11805=CARTESIAN_POINT ( 'NONE',  ( 0.000000000000000000, 5.051668046482832750E-16, -4.000000000000000000 ) ) ;
#11808=ORIENTED_EDGE ( 'NONE', *, *, #4120, .T. ) ;
#11810=EDGE_CURVE ( 'NONE', #12491, #5369, #4896, .T. ) ;
#11819=VECTOR ( 'NONE', #9011, 1000.000000000000000 ) ;
#11841=CARTESIAN_POINT ( 'NONE',  ( 0.000000000000000000, 0.000000000000000000, 0.000000000000000000 ) ) ;
#11848=CIRCLE ( 'NONE', #7659, 4.250000000000000000 ) ;
#11863=TOROIDAL_SURFACE ( 'NONE', #14, 4.000000000000000000, 0.2500000000000000000 ) ;
#11887=VERTEX_POINT ( 'NONE', #4252 ) ;
#11912=CARTESIAN_POINT ( 'NONE',  ( 2.500000000000000000, -1.178949249685214307, 2.042000000000001592 ) ) ;
#11931=LINE ( 'NONE', #6408, #13593 ) ;
#11932=LINE ( 'NONE', #938, #11064 ) ;
#11959=DIRECTION ( 'NONE',  ( -0.5000000000000051070, 0.000000000000000000, 0.8660254037844355990 ) ) ;
#12016=ORIENTED_EDGE ( 'NONE', *, *, #747, .F. ) ;
#12077=ADVANCED_FACE ( 'NONE', ( #5622 ), #13237, .F. ) ;
#12078=DIRECTION ( 'NONE',  ( -1.000000000000000000, -0.000000000000000000, -0.000000000000000000 ) ) ;
#12079=AXIS2_PLACEMENT_3D ( 'NONE', #1546, #9329, #5912 ) ;
#12095=PLANE ( 'NONE',  #7200 ) ;
#12125=ORIENTED_EDGE ( 'NONE', *, *, #6889, .F. ) ;
#12134=DIRECTION ( 'NONE',  ( 0.000000000000000000, -1.224646799147353454E-16, 1.000000000000000000 ) ) ;
#12137=DIRECTION ( 'NONE',  ( 0.000000000000000000, -0.5000000000000013323, -0.8660254037844380415 ) ) ;
#12148=DIRECTION ( 'NONE',  ( 0.000000000000000000, 0.000000000000000000, 1.000000000000000000 ) ) ;
#12158=DIRECTION ( 'NONE',  ( 0.000000000000000000, 0.000000000000000000, -1.000000000000000000 ) ) ;
#12162=CARTESIAN_POINT ( 'NONE',  ( 3.678949249685231848, 0.000000000000000000, 0.000000000000000000 ) ) ;
#12180=CARTESIAN_POINT ( 'NONE',  ( 2.500000000000000000, 1.178949249685212974, -2.042000000000001148 ) ) ;
#12193=DIRECTION ( 'NONE',  ( -0.000000000000000000, 0.000000000000000000, 1.000000000000000000 ) ) ;
#12212=FACE_OUTER_BOUND ( 'NONE', #6384, .T. ) ;
#12217=DIRECTION ( 'NONE',  ( 0.000000000000000000, 0.8660254037844380415, -0.5000000000000012212 ) ) ;
#12228=DIRECTION ( 'NONE',  ( 0.000000000000000000, 0.000000000000000000, -1.000000000000000000 ) ) ;
#12234=ORIENTED_EDGE ( 'NONE', *, *, #9777, .F. ) ;
#12237=EDGE_CURVE ( 'NONE', #2628, #5131, #13575, .T. ) ;
#12287=VERTEX_POINT ( 'NONE', #9312 ) ;
#12316=VECTOR ( 'NONE', #733, 1000.000000000000000 ) ;
#12340=AXIS2_PLACEMENT_3D ( 'NONE', #2141, #6570, #5472 ) ;
#12475=ORIENTED_EDGE ( 'NONE', *, *, #4388, .T. ) ;
#12491=VERTEX_POINT ( 'NONE', #11630 ) ;
#12501=CARTESIAN_POINT ( 'NONE',  ( 0.2500000000000002220, 0.000000000000000000, 4.250000000000000000 ) ) ;
#12508=DIRECTION ( 'NONE',  ( 0.000000000000000000, 0.000000000000000000, 1.000000000000000000 ) ) ;
#12510=VECTOR ( 'NONE', #8126, 1000.000000000000000 ) ;
#12513=EDGE_LOOP ( 'NONE', ( #14004, #170, #8662, #12234, #11430 ) ) ;
#12516=DIRECTION ( 'NONE',  ( 1.000000000000000000, 0.000000000000000000, 0.000000000000000000 ) ) ;
#12533=DIRECTION ( 'NONE',  ( 1.000000000000000000, 0.000000000000000000, 0.000000000000000000 ) ) ;
#12561=EDGE_CURVE ( 'NONE', #12491, #678, #5457, .T. ) ;
#12642=CARTESIAN_POINT ( 'NONE',  ( 2.500000000000000000, 2.357898499370431722, -2.818925648462311528E-15 ) ) ;
#12643=DIRECTION ( 'NONE',  ( 1.000000000000000000, 0.000000000000000000, 0.000000000000000000 ) ) ;
#12656=VECTOR ( 'NONE', #1339, 1000.000000000000000 ) ;
#12662=DIRECTION ( 'NONE',  ( -1.000000000000000000, -0.000000000000000000, -0.000000000000000000 ) ) ;
#12722=CARTESIAN_POINT ( 'NONE',  ( 2.500000000000000000, 2.357898499370431722, -2.818925648462311528E-15 ) ) ;
#12757=EDGE_CURVE ( 'NONE', #4789, #5358, #4732, .T. ) ;
#12763=LINE ( 'NONE', #10520, #1440 ) ;
#12783=EDGE_CURVE ( 'NONE', #8912, #4042, #6824, .T. ) ;
#12810=PLANE ( 'NONE',  #6299 ) ;
#12851=EDGE_LOOP ( 'NONE', ( #9831, #965, #66, #9210, #10160, #4795 ) ) ;
#12853=EDGE_LOOP ( 'NONE', ( #2984, #3902, #2784, #5393, #7783 ) ) ;
#12870=AXIS2_PLACEMENT_3D ( 'NONE', #10277, #305, #10003 ) ;
#12893=EDGE_CURVE ( 'NONE', #4042, #67, #12918, .T. ) ;
#12918=CIRCLE ( 'NONE', #5051, 2.041999999999999815 ) ;
#12928=EDGE_LOOP ( 'NONE', ( #719, #2986, #4092 ) ) ;
#12932=ORIENTED_EDGE ( 'NONE', *, *, #7304, .T. ) ;
#12934=VERTEX_POINT ( 'NONE', #1950 ) ;
#12941=EDGE_LOOP ( 'NONE', ( #9124, #12475, #6686, #11808, #10899 ) ) ;
#12991=CARTESIAN_POINT ( 'NONE',  ( -31.74999999999995737, 0.000000000000000000, 0.000000000000000000 ) ) ;
#13010=CARTESIAN_POINT ( 'NONE',  ( 2.500000000000000000, 1.178949249685212974, -2.042000000000001148 ) ) ;
#13013=DIRECTION ( 'NONE',  ( 0.000000000000000000, 0.4999999999999990008, -0.8660254037844391517 ) ) ;
#13030=CARTESIAN_POINT ( 'NONE',  ( 2.500000000000000000, 2.357898499370431722, -2.818925648462311528E-15 ) ) ;
#13039=ORIENTED_EDGE ( 'NONE', *, *, #12237, .F. ) ;
#13044=CARTESIAN_POINT ( 'NONE',  ( 2.500000000000000000, 2.357898499370431722, -2.818925648462311528E-15 ) ) ;
#13048=ORIENTED_EDGE ( 'NONE', *, *, #2153, .F. ) ;
#13077=DIRECTION ( 'NONE',  ( 0.000000000000000000, -0.5000000000000009992, -0.8660254037844380415 ) ) ;
#13099=ADVANCED_FACE ( 'NONE', ( #1701 ), #4819, .F. ) ;
#13113=DIRECTION ( 'NONE',  ( 0.000000000000000000, -0.4999999999999993339, 0.8660254037844390407 ) ) ;
#13145=ORIENTED_EDGE ( 'NONE', *, *, #8926, .F. ) ;
#13165=CARTESIAN_POINT ( 'NONE',  ( 2.500000000000000000, -1.178949249685214307, 2.042000000000001592 ) ) ;
#13209=EDGE_LOOP ( 'NONE', ( #4133, #14224, #3129, #10818 ) ) ;
#13218=DIRECTION ( 'NONE',  ( -0.7071067811865364705, 0.000000000000000000, 0.7071067811865584529 ) ) ;
#13237=PLANE ( 'NONE',  #8490 ) ;
#13305=DIRECTION ( 'NONE',  ( 0.000000000000000000, 0.000000000000000000, 1.000000000000000000 ) ) ;
#13306=CARTESIAN_POINT ( 'NONE',  ( 2.500000000000000000, -2.357898499370432166, 3.035766082959412415E-15 ) ) ;
#13341=ORIENTED_EDGE ( 'NONE', *, *, #1761, .T. ) ;
#13364=PLANE ( 'NONE',  #3769 ) ;
#13377=EDGE_CURVE ( 'NONE', #5974, #4659, #6676, .T. ) ;
#13575=LINE ( 'NONE', #283, #11739 ) ;
#13592=EDGE_LOOP ( 'NONE', ( #2548, #13039, #13341, #1744, #10758 ) ) ;
#13593=VECTOR ( 'NONE', #3010, 1000.000000000000000 ) ;
#13599=ORIENTED_EDGE ( 'NONE', *, *, #3527, .T. ) ;
#13601=AXIS2_PLACEMENT_3D ( 'NONE', #12991, #8561, #8481 ) ;
#13631=VECTOR ( 'NONE', #11959, 1000.000000000000114 ) ;
#13637=EDGE_CURVE ( 'NONE', #2602, #4143, #11931, .T. ) ;
#13699=( GEOMETRIC_REPRESENTATION_CONTEXT ( 3 ) GLOBAL_UNCERTAINTY_ASSIGNED_CONTEXT ( ( #11613 ) ) GLOBAL_UNIT_ASSIGNED_CONTEXT ( ( #6373, #6298, #762 ) ) REPRESENTATION_CONTEXT ( 'NONE', 'WORKASPACE' ) );
#13720=CARTESIAN_POINT ( 'NONE',  ( 2.500000000000000000, -1.768423874527825568, -1.020999999999998575 ) ) ;
#13765=EDGE_CURVE ( 'NONE', #5358, #1004, #2482, .T. ) ;
#13766=DIRECTION ( 'NONE',  ( -1.000000000000000000, -0.000000000000000000, -0.000000000000000000 ) ) ;
#13781=PRODUCT_DEFINITION_CONTEXT ( 'detailed design', #1632, 'design' ) ;
#13796=CARTESIAN_POINT ( 'NONE',  ( 2.500000000000000000, 2.357898499370431722, -2.818925648462311528E-15 ) ) ;
#13800=DIRECTION ( 'NONE',  ( 1.000000000000000000, 0.000000000000000000, 0.000000000000000000 ) ) ;
#13801=DIRECTION ( 'NONE',  ( 0.000000000000000000, 1.000000000000000000, -1.224646799147353207E-16 ) ) ;
#13804=ORIENTED_EDGE ( 'NONE', *, *, #10475, .T. ) ;
#13825=AXIS2_PLACEMENT_3D ( 'NONE', #6133, #1549, #11501 ) ;
#13837=PLANE ( 'NONE',  #5085 ) ;
#13898=DIRECTION ( 'NONE',  ( 0.000000000000000000, 0.000000000000000000, 1.000000000000000000 ) ) ;
#13917=ADVANCED_FACE ( 'NONE', ( #9221 ), #7043, .F. ) ;
#13923=DIRECTION ( 'NONE',  ( 0.000000000000000000, -0.4999999999999993339, 0.8660254037844390407 ) ) ;
#13932=DIRECTION ( 'NONE',  ( -1.000000000000000000, -0.000000000000000000, -0.000000000000000000 ) ) ;
#13956=LINE ( 'NONE', #2272, #4937 ) ;
#13963=DIRECTION ( 'NONE',  ( 0.000000000000000000, 0.000000000000000000, -1.000000000000000000 ) ) ;
#13989=DIRECTION ( 'NONE',  ( -1.000000000000000000, -0.000000000000000000, -0.000000000000000000 ) ) ;
#14001=ORIENTED_EDGE ( 'NONE', *, *, #14011, .F. ) ;
#14004=ORIENTED_EDGE ( 'NONE', *, *, #3806, .T. ) ;
#14011=EDGE_CURVE ( 'NONE', #5369, #12491, #11750, .T. ) ;
#14028=ADVANCED_FACE ( 'NONE', ( #1660 ), #6101, .T. ) ;
#14031=EDGE_CURVE ( 'NONE', #4659, #11887, #5017, .T. ) ;
#14039=AXIS2_PLACEMENT_3D ( 'NONE', #10508, #9418, #5077 ) ;
#14053=CARTESIAN_POINT ( 'NONE',  ( 2.500000000000000000, 0.000000000000000000, 2.041999999999999815 ) ) ;
#14067=ORIENTED_EDGE ( 'NONE', *, *, #9777, .T. ) ;
#14174=CIRCLE ( 'NONE', #10727, 2.500000000000000444 ) ;
#14182=EDGE_CURVE ( 'NONE', #67, #4723, #11767, .T. ) ;
#14202=CARTESIAN_POINT ( 'NONE',  ( 2.500000000000000000, 2.357898499370431722, -2.818925648462311528E-15 ) ) ;
#14224=ORIENTED_EDGE ( 'NONE', *, *, #12757, .T. ) ;
#14230=DIRECTION ( 'NONE',  ( -1.000000000000000000, -0.000000000000000000, -0.000000000000000000 ) ) ;
#14254=CARTESIAN_POINT ( 'NONE',  ( 0.000000000000000000, 0.000000000000000000, 0.000000000000000000 ) ) ;
#14259=VECTOR ( 'NONE', #11168, 1000.000000000000000 ) ;
#14289=EDGE_LOOP ( 'NONE', ( #3807, #12125, #5031, #7421, #6058 ) ) ;
#14305=LINE ( 'NONE', #4307, #7796 ) ;
#14411=COLOUR_RGB('Black',0.12,0.14,0.17);
#14412=FILL_AREA_STYLE_COLOUR('',#14411);
#14413=FILL_AREA_STYLE('',(#14412));
#14414=SURFACE_STYLE_FILL_AREA(#14413);
#14415=SURFACE_SIDE_STYLE('',(#14414));
#14416=SURFACE_STYLE_USAGE(.BOTH.,#14415);
#14417=PRESENTATION_STYLE_ASSIGNMENT((#14416));
ENDSEC;
END-ISO-10303-21;
